ISO-10303-21;
HEADER;
/* Generated by software containing ST-Developer
 * from STEP Tools, Inc. (www.steptools.com) 
 */

FILE_DESCRIPTION(
/* description */ ('Bin tilter linkage'),
/* implementation_level */ '2;1');

FILE_NAME(
/* name */ 'Input link (1).step',
/* time_stamp */ '2026-10-28T03:26:24-07:00',
/* author */ (''),
/* organization */ (''),
/* preprocessor_version */ 'ST-DEVELOPER v20.2',
/* originating_system */ 'Autodesk Translation Framework v15.17.0.0',
/* authorisation */ '');

FILE_SCHEMA (('AUTOMOTIVE_DESIGN { 1 0 10303 214 3 1 1 }'));
ENDSEC;

DATA;
#10=MECHANICAL_DESIGN_GEOMETRIC_PRESENTATION_REPRESENTATION('',(#892),#23728);
#680=SHAPE_REPRESENTATION_RELATIONSHIP('SRR','None',#24145,#786);
#786=ADVANCED_BREP_SHAPE_REPRESENTATION('',(#1005),#23645);
#892=STYLED_ITEM('',(#24779),#1005);
#1005=MANIFOLD_SOLID_BREP('Body1',#12423);
#1234=FACE_BOUND('',#3070,.T.);
#1235=FACE_BOUND('',#3071,.T.);
#1236=FACE_BOUND('',#3072,.T.);
#1237=FACE_BOUND('',#3073,.T.);
#1238=FACE_BOUND('',#3074,.T.);
#1239=FACE_BOUND('',#3075,.T.);
#1240=FACE_BOUND('',#3076,.T.);
#1241=FACE_BOUND('',#3077,.T.);
#1242=FACE_BOUND('',#3078,.T.);
#1243=FACE_BOUND('',#3079,.T.);
#1244=FACE_BOUND('',#3089,.T.);
#1245=FACE_BOUND('',#3090,.T.);
#1246=FACE_BOUND('',#3091,.T.);
#1247=FACE_BOUND('',#3092,.T.);
#1248=FACE_BOUND('',#3093,.T.);
#1249=FACE_BOUND('',#3094,.T.);
#1250=FACE_BOUND('',#3095,.T.);
#1251=FACE_BOUND('',#3096,.T.);
#1252=FACE_BOUND('',#3097,.T.);
#1253=FACE_BOUND('',#3098,.T.);
#1617=PLANE('',#14221);
#1618=PLANE('',#14228);
#1619=PLANE('',#14241);
#1620=PLANE('',#14242);
#2139=FACE_OUTER_BOUND('',#3063,.T.);
#2140=FACE_OUTER_BOUND('',#3064,.T.);
#2141=FACE_OUTER_BOUND('',#3065,.T.);
#2142=FACE_OUTER_BOUND('',#3066,.T.);
#2143=FACE_OUTER_BOUND('',#3067,.T.);
#2144=FACE_OUTER_BOUND('',#3068,.T.);
#2145=FACE_OUTER_BOUND('',#3069,.T.);
#2146=FACE_OUTER_BOUND('',#3080,.T.);
#2147=FACE_OUTER_BOUND('',#3081,.T.);
#2148=FACE_OUTER_BOUND('',#3082,.T.);
#2149=FACE_OUTER_BOUND('',#3083,.T.);
#2150=FACE_OUTER_BOUND('',#3084,.T.);
#2151=FACE_OUTER_BOUND('',#3085,.T.);
#2152=FACE_OUTER_BOUND('',#3086,.T.);
#2153=FACE_OUTER_BOUND('',#3087,.T.);
#2154=FACE_OUTER_BOUND('',#3088,.T.);
#3063=EDGE_LOOP('',(#9373,#9374,#9375,#9376));
#3064=EDGE_LOOP('',(#9377,#9378,#9379,#9380));
#3065=EDGE_LOOP('',(#9381,#9382,#9383,#9384));
#3066=EDGE_LOOP('',(#9385,#9386,#9387,#9388));
#3067=EDGE_LOOP('',(#9389,#9390,#9391,#9392));
#3068=EDGE_LOOP('',(#9393,#9394,#9395,#9396));
#3069=EDGE_LOOP('',(#9397,#9398,#9399,#9400));
#3070=EDGE_LOOP('',(#9401));
#3071=EDGE_LOOP('',(#9402));
#3072=EDGE_LOOP('',(#9403));
#3073=EDGE_LOOP('',(#9404));
#3074=EDGE_LOOP('',(#9405));
#3075=EDGE_LOOP('',(#9406));
#3076=EDGE_LOOP('',(#9407));
#3077=EDGE_LOOP('',(#9408));
#3078=EDGE_LOOP('',(#9409));
#3079=EDGE_LOOP('',(#9410));
#3080=EDGE_LOOP('',(#9411,#9412,#9413,#9414));
#3081=EDGE_LOOP('',(#9415,#9416,#9417,#9418));
#3082=EDGE_LOOP('',(#9419,#9420,#9421,#9422));
#3083=EDGE_LOOP('',(#9423,#9424,#9425,#9426));
#3084=EDGE_LOOP('',(#9427,#9428,#9429,#9430));
#3085=EDGE_LOOP('',(#9431,#9432,#9433,#9434));
#3086=EDGE_LOOP('',(#9435,#9436,#9437,#9438));
#3087=EDGE_LOOP('',(#9439,#9440,#9441,#9442));
#3088=EDGE_LOOP('',(#9443,#9444,#9445,#9446));
#3089=EDGE_LOOP('',(#9447));
#3090=EDGE_LOOP('',(#9448));
#3091=EDGE_LOOP('',(#9449));
#3092=EDGE_LOOP('',(#9450));
#3093=EDGE_LOOP('',(#9451));
#3094=EDGE_LOOP('',(#9452));
#3095=EDGE_LOOP('',(#9453));
#3096=EDGE_LOOP('',(#9454));
#3097=EDGE_LOOP('',(#9455));
#3098=EDGE_LOOP('',(#9456));
#4105=LINE('',#20864,#4780);
#4106=LINE('',#20870,#4781);
#4107=LINE('',#20876,#4782);
#4108=LINE('',#20882,#4783);
#4109=LINE('',#20888,#4784);
#4110=LINE('',#20893,#4785);
#4111=LINE('',#20897,#4786);
#4112=LINE('',#20901,#4787);
#4113=LINE('',#20904,#4788);
#4114=LINE('',#20917,#4789);
#4115=LINE('',#20918,#4790);
#4116=LINE('',#20921,#4791);
#4117=LINE('',#20925,#4792);
#4118=LINE('',#20929,#4793);
#4119=LINE('',#20933,#4794);
#4120=LINE('',#20937,#4795);
#4121=LINE('',#20941,#4796);
#4122=LINE('',#20944,#4797);
#4780=VECTOR('',#16788,0.164999999999999);
#4781=VECTOR('',#16795,0.164999999999999);
#4782=VECTOR('',#16802,0.164999999999999);
#4783=VECTOR('',#16809,0.164999999999999);
#4784=VECTOR('',#16816,1.6);
#4785=VECTOR('',#16821,1.);
#4786=VECTOR('',#16824,1.);
#4787=VECTOR('',#16829,1.);
#4788=VECTOR('',#16832,1.);
#4789=VECTOR('',#16845,1.);
#4790=VECTOR('',#16846,1.);
#4791=VECTOR('',#16849,0.165);
#4792=VECTOR('',#16854,0.165);
#4793=VECTOR('',#16859,0.165);
#4794=VECTOR('',#16864,0.165);
#4795=VECTOR('',#16869,1.6);
#4796=VECTOR('',#16874,1.);
#4797=VECTOR('',#16879,1.);
#5443=CIRCLE('',#14204,0.164999999999999);
#5444=CIRCLE('',#14205,0.164999999999999);
#5445=CIRCLE('',#14207,0.164999999999999);
#5446=CIRCLE('',#14208,0.164999999999999);
#5447=CIRCLE('',#14210,0.164999999999999);
#5448=CIRCLE('',#14211,0.164999999999999);
#5449=CIRCLE('',#14213,0.164999999999999);
#5450=CIRCLE('',#14214,0.164999999999999);
#5451=CIRCLE('',#14216,1.6);
#5452=CIRCLE('',#14217,1.6);
#5453=CIRCLE('',#14219,2.2);
#5454=CIRCLE('',#14220,2.2);
#5455=CIRCLE('',#14222,2.2);
#5456=CIRCLE('',#14223,1.6);
#5457=CIRCLE('',#14224,0.165);
#5458=CIRCLE('',#14225,0.165);
#5459=CIRCLE('',#14226,0.165);
#5460=CIRCLE('',#14227,0.165);
#5461=CIRCLE('',#14230,0.165);
#5462=CIRCLE('',#14232,0.165);
#5463=CIRCLE('',#14234,0.165);
#5464=CIRCLE('',#14236,0.165);
#5465=CIRCLE('',#14238,1.6);
#5466=CIRCLE('',#14240,2.2);
#6289=VERTEX_POINT('',#20861);
#6290=VERTEX_POINT('',#20863);
#6291=VERTEX_POINT('',#20867);
#6292=VERTEX_POINT('',#20869);
#6293=VERTEX_POINT('',#20873);
#6294=VERTEX_POINT('',#20875);
#6295=VERTEX_POINT('',#20879);
#6296=VERTEX_POINT('',#20881);
#6297=VERTEX_POINT('',#20885);
#6298=VERTEX_POINT('',#20887);
#6299=VERTEX_POINT('',#20891);
#6300=VERTEX_POINT('',#20892);
#6301=VERTEX_POINT('',#20894);
#6302=VERTEX_POINT('',#20896);
#6303=VERTEX_POINT('',#20900);
#6304=VERTEX_POINT('',#20902);
#6305=VERTEX_POINT('',#20905);
#6306=VERTEX_POINT('',#20907);
#6307=VERTEX_POINT('',#20909);
#6308=VERTEX_POINT('',#20911);
#6309=VERTEX_POINT('',#20913);
#6310=VERTEX_POINT('',#20916);
#6311=VERTEX_POINT('',#20920);
#6312=VERTEX_POINT('',#20924);
#6313=VERTEX_POINT('',#20928);
#6314=VERTEX_POINT('',#20932);
#6315=VERTEX_POINT('',#20936);
#6316=VERTEX_POINT('',#20940);
#7426=EDGE_CURVE('',#6289,#6289,#5443,.T.);
#7427=EDGE_CURVE('',#6289,#6290,#4105,.T.);
#7428=EDGE_CURVE('',#6290,#6290,#5444,.T.);
#7429=EDGE_CURVE('',#6291,#6291,#5445,.T.);
#7430=EDGE_CURVE('',#6291,#6292,#4106,.T.);
#7431=EDGE_CURVE('',#6292,#6292,#5446,.T.);
#7432=EDGE_CURVE('',#6293,#6293,#5447,.T.);
#7433=EDGE_CURVE('',#6293,#6294,#4107,.T.);
#7434=EDGE_CURVE('',#6294,#6294,#5448,.T.);
#7435=EDGE_CURVE('',#6295,#6295,#5449,.T.);
#7436=EDGE_CURVE('',#6295,#6296,#4108,.T.);
#7437=EDGE_CURVE('',#6296,#6296,#5450,.T.);
#7438=EDGE_CURVE('',#6297,#6297,#5451,.T.);
#7439=EDGE_CURVE('',#6297,#6298,#4109,.T.);
#7440=EDGE_CURVE('',#6298,#6298,#5452,.T.);
#7441=EDGE_CURVE('',#6299,#6300,#4110,.T.);
#7442=EDGE_CURVE('',#6301,#6299,#5453,.T.);
#7443=EDGE_CURVE('',#6302,#6301,#4111,.T.);
#7444=EDGE_CURVE('',#6302,#6300,#5454,.T.);
#7445=EDGE_CURVE('',#6303,#6302,#4112,.T.);
#7446=EDGE_CURVE('',#6304,#6303,#5455,.T.);
#7447=EDGE_CURVE('',#6300,#6304,#4113,.T.);
#7448=EDGE_CURVE('',#6305,#6305,#5456,.T.);
#7449=EDGE_CURVE('',#6306,#6306,#5457,.T.);
#7450=EDGE_CURVE('',#6307,#6307,#5458,.T.);
#7451=EDGE_CURVE('',#6308,#6308,#5459,.T.);
#7452=EDGE_CURVE('',#6309,#6309,#5460,.T.);
#7453=EDGE_CURVE('',#6310,#6301,#4114,.T.);
#7454=EDGE_CURVE('',#6310,#6303,#4115,.T.);
#7455=EDGE_CURVE('',#6309,#6311,#4116,.T.);
#7456=EDGE_CURVE('',#6311,#6311,#5461,.T.);
#7457=EDGE_CURVE('',#6308,#6312,#4117,.T.);
#7458=EDGE_CURVE('',#6312,#6312,#5462,.T.);
#7459=EDGE_CURVE('',#6307,#6313,#4118,.T.);
#7460=EDGE_CURVE('',#6313,#6313,#5463,.T.);
#7461=EDGE_CURVE('',#6306,#6314,#4119,.T.);
#7462=EDGE_CURVE('',#6314,#6314,#5464,.T.);
#7463=EDGE_CURVE('',#6305,#6315,#4120,.T.);
#7464=EDGE_CURVE('',#6315,#6315,#5465,.T.);
#7465=EDGE_CURVE('',#6304,#6316,#4121,.T.);
#7466=EDGE_CURVE('',#6316,#6310,#5466,.T.);
#7467=EDGE_CURVE('',#6299,#6316,#4122,.T.);
#9373=ORIENTED_EDGE('',*,*,#7426,.F.);
#9374=ORIENTED_EDGE('',*,*,#7427,.T.);
#9375=ORIENTED_EDGE('',*,*,#7428,.F.);
#9376=ORIENTED_EDGE('',*,*,#7427,.F.);
#9377=ORIENTED_EDGE('',*,*,#7429,.F.);
#9378=ORIENTED_EDGE('',*,*,#7430,.T.);
#9379=ORIENTED_EDGE('',*,*,#7431,.F.);
#9380=ORIENTED_EDGE('',*,*,#7430,.F.);
#9381=ORIENTED_EDGE('',*,*,#7432,.F.);
#9382=ORIENTED_EDGE('',*,*,#7433,.T.);
#9383=ORIENTED_EDGE('',*,*,#7434,.F.);
#9384=ORIENTED_EDGE('',*,*,#7433,.F.);
#9385=ORIENTED_EDGE('',*,*,#7435,.F.);
#9386=ORIENTED_EDGE('',*,*,#7436,.T.);
#9387=ORIENTED_EDGE('',*,*,#7437,.F.);
#9388=ORIENTED_EDGE('',*,*,#7436,.F.);
#9389=ORIENTED_EDGE('',*,*,#7438,.F.);
#9390=ORIENTED_EDGE('',*,*,#7439,.T.);
#9391=ORIENTED_EDGE('',*,*,#7440,.F.);
#9392=ORIENTED_EDGE('',*,*,#7439,.F.);
#9393=ORIENTED_EDGE('',*,*,#7441,.F.);
#9394=ORIENTED_EDGE('',*,*,#7442,.F.);
#9395=ORIENTED_EDGE('',*,*,#7443,.F.);
#9396=ORIENTED_EDGE('',*,*,#7444,.T.);
#9397=ORIENTED_EDGE('',*,*,#7444,.F.);
#9398=ORIENTED_EDGE('',*,*,#7445,.F.);
#9399=ORIENTED_EDGE('',*,*,#7446,.F.);
#9400=ORIENTED_EDGE('',*,*,#7447,.F.);
#9401=ORIENTED_EDGE('',*,*,#7448,.T.);
#9402=ORIENTED_EDGE('',*,*,#7449,.T.);
#9403=ORIENTED_EDGE('',*,*,#7450,.T.);
#9404=ORIENTED_EDGE('',*,*,#7451,.T.);
#9405=ORIENTED_EDGE('',*,*,#7452,.T.);
#9406=ORIENTED_EDGE('',*,*,#7438,.T.);
#9407=ORIENTED_EDGE('',*,*,#7435,.T.);
#9408=ORIENTED_EDGE('',*,*,#7432,.T.);
#9409=ORIENTED_EDGE('',*,*,#7429,.T.);
#9410=ORIENTED_EDGE('',*,*,#7426,.T.);
#9411=ORIENTED_EDGE('',*,*,#7443,.T.);
#9412=ORIENTED_EDGE('',*,*,#7453,.F.);
#9413=ORIENTED_EDGE('',*,*,#7454,.T.);
#9414=ORIENTED_EDGE('',*,*,#7445,.T.);
#9415=ORIENTED_EDGE('',*,*,#7452,.F.);
#9416=ORIENTED_EDGE('',*,*,#7455,.T.);
#9417=ORIENTED_EDGE('',*,*,#7456,.F.);
#9418=ORIENTED_EDGE('',*,*,#7455,.F.);
#9419=ORIENTED_EDGE('',*,*,#7451,.F.);
#9420=ORIENTED_EDGE('',*,*,#7457,.T.);
#9421=ORIENTED_EDGE('',*,*,#7458,.F.);
#9422=ORIENTED_EDGE('',*,*,#7457,.F.);
#9423=ORIENTED_EDGE('',*,*,#7450,.F.);
#9424=ORIENTED_EDGE('',*,*,#7459,.T.);
#9425=ORIENTED_EDGE('',*,*,#7460,.F.);
#9426=ORIENTED_EDGE('',*,*,#7459,.F.);
#9427=ORIENTED_EDGE('',*,*,#7449,.F.);
#9428=ORIENTED_EDGE('',*,*,#7461,.T.);
#9429=ORIENTED_EDGE('',*,*,#7462,.F.);
#9430=ORIENTED_EDGE('',*,*,#7461,.F.);
#9431=ORIENTED_EDGE('',*,*,#7448,.F.);
#9432=ORIENTED_EDGE('',*,*,#7463,.T.);
#9433=ORIENTED_EDGE('',*,*,#7464,.F.);
#9434=ORIENTED_EDGE('',*,*,#7463,.F.);
#9435=ORIENTED_EDGE('',*,*,#7465,.F.);
#9436=ORIENTED_EDGE('',*,*,#7446,.T.);
#9437=ORIENTED_EDGE('',*,*,#7454,.F.);
#9438=ORIENTED_EDGE('',*,*,#7466,.F.);
#9439=ORIENTED_EDGE('',*,*,#7441,.T.);
#9440=ORIENTED_EDGE('',*,*,#7447,.T.);
#9441=ORIENTED_EDGE('',*,*,#7465,.T.);
#9442=ORIENTED_EDGE('',*,*,#7467,.F.);
#9443=ORIENTED_EDGE('',*,*,#7467,.T.);
#9444=ORIENTED_EDGE('',*,*,#7466,.T.);
#9445=ORIENTED_EDGE('',*,*,#7453,.T.);
#9446=ORIENTED_EDGE('',*,*,#7442,.T.);
#9447=ORIENTED_EDGE('',*,*,#7456,.T.);
#9448=ORIENTED_EDGE('',*,*,#7458,.T.);
#9449=ORIENTED_EDGE('',*,*,#7460,.T.);
#9450=ORIENTED_EDGE('',*,*,#7462,.T.);
#9451=ORIENTED_EDGE('',*,*,#7464,.T.);
#9452=ORIENTED_EDGE('',*,*,#7440,.T.);
#9453=ORIENTED_EDGE('',*,*,#7437,.T.);
#9454=ORIENTED_EDGE('',*,*,#7434,.T.);
#9455=ORIENTED_EDGE('',*,*,#7431,.T.);
#9456=ORIENTED_EDGE('',*,*,#7428,.T.);
#11387=CYLINDRICAL_SURFACE('',#14203,0.164999999999999);
#11388=CYLINDRICAL_SURFACE('',#14206,0.164999999999999);
#11389=CYLINDRICAL_SURFACE('',#14209,0.164999999999999);
#11390=CYLINDRICAL_SURFACE('',#14212,0.164999999999999);
#11391=CYLINDRICAL_SURFACE('',#14215,1.6);
#11392=CYLINDRICAL_SURFACE('',#14218,2.2);
#11393=CYLINDRICAL_SURFACE('',#14229,0.165);
#11394=CYLINDRICAL_SURFACE('',#14231,0.165);
#11395=CYLINDRICAL_SURFACE('',#14233,0.165);
#11396=CYLINDRICAL_SURFACE('',#14235,0.165);
#11397=CYLINDRICAL_SURFACE('',#14237,1.6);
#11398=CYLINDRICAL_SURFACE('',#14239,2.2);
#11864=ADVANCED_FACE('',(#2139),#11387,.F.);
#11865=ADVANCED_FACE('',(#2140),#11388,.F.);
#11866=ADVANCED_FACE('',(#2141),#11389,.F.);
#11867=ADVANCED_FACE('',(#2142),#11390,.F.);
#11868=ADVANCED_FACE('',(#2143),#11391,.F.);
#11869=ADVANCED_FACE('',(#2144),#11392,.T.);
#11870=ADVANCED_FACE('',(#2145,#1234,#1235,#1236,#1237,#1238,#1239,#1240,
#1241,#1242,#1243),#1617,.F.);
#11871=ADVANCED_FACE('',(#2146),#1618,.T.);
#11872=ADVANCED_FACE('',(#2147),#11393,.F.);
#11873=ADVANCED_FACE('',(#2148),#11394,.F.);
#11874=ADVANCED_FACE('',(#2149),#11395,.F.);
#11875=ADVANCED_FACE('',(#2150),#11396,.F.);
#11876=ADVANCED_FACE('',(#2151),#11397,.F.);
#11877=ADVANCED_FACE('',(#2152),#11398,.T.);
#11878=ADVANCED_FACE('',(#2153),#1619,.T.);
#11879=ADVANCED_FACE('',(#2154,#1244,#1245,#1246,#1247,#1248,#1249,#1250,
#1251,#1252,#1253),#1620,.T.);
#12423=CLOSED_SHELL('',(#11864,#11865,#11866,#11867,#11868,#11869,#11870,
#11871,#11872,#11873,#11874,#11875,#11876,#11877,#11878,#11879));
#14202=AXIS2_PLACEMENT_3D('',#20859,#16782,#16783);
#14203=AXIS2_PLACEMENT_3D('',#20860,#16784,#16785);
#14204=AXIS2_PLACEMENT_3D('',#20862,#16786,#16787);
#14205=AXIS2_PLACEMENT_3D('',#20865,#16789,#16790);
#14206=AXIS2_PLACEMENT_3D('',#20866,#16791,#16792);
#14207=AXIS2_PLACEMENT_3D('',#20868,#16793,#16794);
#14208=AXIS2_PLACEMENT_3D('',#20871,#16796,#16797);
#14209=AXIS2_PLACEMENT_3D('',#20872,#16798,#16799);
#14210=AXIS2_PLACEMENT_3D('',#20874,#16800,#16801);
#14211=AXIS2_PLACEMENT_3D('',#20877,#16803,#16804);
#14212=AXIS2_PLACEMENT_3D('',#20878,#16805,#16806);
#14213=AXIS2_PLACEMENT_3D('',#20880,#16807,#16808);
#14214=AXIS2_PLACEMENT_3D('',#20883,#16810,#16811);
#14215=AXIS2_PLACEMENT_3D('',#20884,#16812,#16813);
#14216=AXIS2_PLACEMENT_3D('',#20886,#16814,#16815);
#14217=AXIS2_PLACEMENT_3D('',#20889,#16817,#16818);
#14218=AXIS2_PLACEMENT_3D('',#20890,#16819,#16820);
#14219=AXIS2_PLACEMENT_3D('',#20895,#16822,#16823);
#14220=AXIS2_PLACEMENT_3D('',#20898,#16825,#16826);
#14221=AXIS2_PLACEMENT_3D('',#20899,#16827,#16828);
#14222=AXIS2_PLACEMENT_3D('',#20903,#16830,#16831);
#14223=AXIS2_PLACEMENT_3D('',#20906,#16833,#16834);
#14224=AXIS2_PLACEMENT_3D('',#20908,#16835,#16836);
#14225=AXIS2_PLACEMENT_3D('',#20910,#16837,#16838);
#14226=AXIS2_PLACEMENT_3D('',#20912,#16839,#16840);
#14227=AXIS2_PLACEMENT_3D('',#20914,#16841,#16842);
#14228=AXIS2_PLACEMENT_3D('',#20915,#16843,#16844);
#14229=AXIS2_PLACEMENT_3D('',#20919,#16847,#16848);
#14230=AXIS2_PLACEMENT_3D('',#20922,#16850,#16851);
#14231=AXIS2_PLACEMENT_3D('',#20923,#16852,#16853);
#14232=AXIS2_PLACEMENT_3D('',#20926,#16855,#16856);
#14233=AXIS2_PLACEMENT_3D('',#20927,#16857,#16858);
#14234=AXIS2_PLACEMENT_3D('',#20930,#16860,#16861);
#14235=AXIS2_PLACEMENT_3D('',#20931,#16862,#16863);
#14236=AXIS2_PLACEMENT_3D('',#20934,#16865,#16866);
#14237=AXIS2_PLACEMENT_3D('',#20935,#16867,#16868);
#14238=AXIS2_PLACEMENT_3D('',#20938,#16870,#16871);
#14239=AXIS2_PLACEMENT_3D('',#20939,#16872,#16873);
#14240=AXIS2_PLACEMENT_3D('',#20942,#16875,#16876);
#14241=AXIS2_PLACEMENT_3D('',#20943,#16877,#16878);
#14242=AXIS2_PLACEMENT_3D('',#20945,#16880,#16881);
#16782=DIRECTION('axis',(0.,0.,1.));
#16783=DIRECTION('refdir',(1.,0.,0.));
#16784=DIRECTION('center_axis',(0.,1.,0.));
#16785=DIRECTION('ref_axis',(1.,0.,0.));
#16786=DIRECTION('center_axis',(0.,1.,0.));
#16787=DIRECTION('ref_axis',(1.,0.,0.));
#16788=DIRECTION('',(0.,1.,0.));
#16789=DIRECTION('center_axis',(0.,-1.,0.));
#16790=DIRECTION('ref_axis',(1.,0.,0.));
#16791=DIRECTION('center_axis',(0.,1.,0.));
#16792=DIRECTION('ref_axis',(1.,0.,0.));
#16793=DIRECTION('center_axis',(0.,1.,0.));
#16794=DIRECTION('ref_axis',(1.,0.,0.));
#16795=DIRECTION('',(0.,1.,0.));
#16796=DIRECTION('center_axis',(0.,-1.,0.));
#16797=DIRECTION('ref_axis',(1.,0.,0.));
#16798=DIRECTION('center_axis',(0.,1.,0.));
#16799=DIRECTION('ref_axis',(1.,0.,0.));
#16800=DIRECTION('center_axis',(0.,1.,0.));
#16801=DIRECTION('ref_axis',(1.,0.,0.));
#16802=DIRECTION('',(0.,1.,0.));
#16803=DIRECTION('center_axis',(0.,-1.,0.));
#16804=DIRECTION('ref_axis',(1.,0.,0.));
#16805=DIRECTION('center_axis',(0.,1.,0.));
#16806=DIRECTION('ref_axis',(1.,0.,0.));
#16807=DIRECTION('center_axis',(0.,1.,0.));
#16808=DIRECTION('ref_axis',(1.,0.,0.));
#16809=DIRECTION('',(0.,1.,0.));
#16810=DIRECTION('center_axis',(0.,-1.,0.));
#16811=DIRECTION('ref_axis',(1.,0.,0.));
#16812=DIRECTION('center_axis',(0.,1.,0.));
#16813=DIRECTION('ref_axis',(1.,0.,0.));
#16814=DIRECTION('center_axis',(0.,1.,0.));
#16815=DIRECTION('ref_axis',(1.,0.,0.));
#16816=DIRECTION('',(0.,1.,0.));
#16817=DIRECTION('center_axis',(0.,-1.,0.));
#16818=DIRECTION('ref_axis',(1.,0.,0.));
#16819=DIRECTION('center_axis',(0.,1.,0.));
#16820=DIRECTION('ref_axis',(1.,0.,0.));
#16821=DIRECTION('',(0.,-1.,0.));
#16822=DIRECTION('center_axis',(0.,1.,0.));
#16823=DIRECTION('ref_axis',(1.,0.,0.));
#16824=DIRECTION('',(0.,1.,0.));
#16825=DIRECTION('center_axis',(0.,1.,0.));
#16826=DIRECTION('ref_axis',(1.,0.,0.));
#16827=DIRECTION('center_axis',(0.,1.,0.));
#16828=DIRECTION('ref_axis',(1.,0.,0.));
#16829=DIRECTION('',(0.939692620785908,0.,0.342020143325669));
#16830=DIRECTION('center_axis',(0.,1.,0.));
#16831=DIRECTION('ref_axis',(1.,0.,0.));
#16832=DIRECTION('',(-0.939692620785909,0.,-0.342020143325669));
#16833=DIRECTION('center_axis',(0.,1.,0.));
#16834=DIRECTION('ref_axis',(1.,0.,0.));
#16835=DIRECTION('center_axis',(0.,1.,0.));
#16836=DIRECTION('ref_axis',(1.,0.,0.));
#16837=DIRECTION('center_axis',(0.,1.,0.));
#16838=DIRECTION('ref_axis',(1.,0.,0.));
#16839=DIRECTION('center_axis',(0.,1.,0.));
#16840=DIRECTION('ref_axis',(1.,0.,0.));
#16841=DIRECTION('center_axis',(0.,1.,0.));
#16842=DIRECTION('ref_axis',(1.,0.,0.));
#16843=DIRECTION('center_axis',(-0.342020143325669,0.,0.939692620785908));
#16844=DIRECTION('ref_axis',(0.939692620785908,0.,0.342020143325669));
#16845=DIRECTION('',(0.939692620785908,0.,0.342020143325669));
#16846=DIRECTION('',(0.,-1.,0.));
#16847=DIRECTION('center_axis',(0.,1.,0.));
#16848=DIRECTION('ref_axis',(1.,0.,0.));
#16849=DIRECTION('',(0.,1.,0.));
#16850=DIRECTION('center_axis',(0.,-1.,0.));
#16851=DIRECTION('ref_axis',(1.,0.,0.));
#16852=DIRECTION('center_axis',(0.,1.,0.));
#16853=DIRECTION('ref_axis',(1.,0.,0.));
#16854=DIRECTION('',(0.,1.,0.));
#16855=DIRECTION('center_axis',(0.,-1.,0.));
#16856=DIRECTION('ref_axis',(1.,0.,0.));
#16857=DIRECTION('center_axis',(0.,1.,0.));
#16858=DIRECTION('ref_axis',(1.,0.,0.));
#16859=DIRECTION('',(0.,1.,0.));
#16860=DIRECTION('center_axis',(0.,-1.,0.));
#16861=DIRECTION('ref_axis',(1.,0.,0.));
#16862=DIRECTION('center_axis',(0.,1.,0.));
#16863=DIRECTION('ref_axis',(1.,0.,0.));
#16864=DIRECTION('',(0.,1.,0.));
#16865=DIRECTION('center_axis',(0.,-1.,0.));
#16866=DIRECTION('ref_axis',(1.,0.,0.));
#16867=DIRECTION('center_axis',(0.,1.,0.));
#16868=DIRECTION('ref_axis',(1.,0.,0.));
#16869=DIRECTION('',(0.,1.,0.));
#16870=DIRECTION('center_axis',(0.,-1.,0.));
#16871=DIRECTION('ref_axis',(1.,0.,0.));
#16872=DIRECTION('center_axis',(0.,1.,0.));
#16873=DIRECTION('ref_axis',(-0.939692620785908,0.,-0.342020143325669));
#16874=DIRECTION('',(0.,1.,0.));
#16875=DIRECTION('center_axis',(0.,1.,0.));
#16876=DIRECTION('ref_axis',(1.,0.,0.));
#16877=DIRECTION('center_axis',(0.342020143325669,0.,-0.939692620785909));
#16878=DIRECTION('ref_axis',(-0.939692620785909,0.,-0.342020143325669));
#16879=DIRECTION('',(-0.939692620785909,0.,-0.342020143325669));
#16880=DIRECTION('center_axis',(0.,1.,0.));
#16881=DIRECTION('ref_axis',(0.,0.,1.));
#20859=CARTESIAN_POINT('',(0.,0.,0.));
#20860=CARTESIAN_POINT('Origin',(8.08877866266397,-0.6,17.1120538880616));
#20861=CARTESIAN_POINT('',(7.92377866266397,-0.5,17.1120538880616));
#20862=CARTESIAN_POINT('Origin',(8.08877866266397,-0.5,17.1120538880616));
#20863=CARTESIAN_POINT('',(7.92377866266397,0.5,17.1120538880616));
#20864=CARTESIAN_POINT('',(7.92377866266397,-0.6,17.1120538880616));
#20865=CARTESIAN_POINT('Origin',(8.08877866266397,0.5,17.1120538880616));
#20866=CARTESIAN_POINT('Origin',(8.08877866266397,-0.6,19.7283489784518));
#20867=CARTESIAN_POINT('',(7.92377866266397,-0.5,19.7283489784518));
#20868=CARTESIAN_POINT('Origin',(8.08877866266397,-0.5,19.7283489784518));
#20869=CARTESIAN_POINT('',(7.92377866266397,0.5,19.7283489784518));
#20870=CARTESIAN_POINT('',(7.92377866266397,-0.6,19.7283489784518));
#20871=CARTESIAN_POINT('Origin',(8.08877866266397,0.5,19.7283489784518));
#20872=CARTESIAN_POINT('Origin',(10.7050737530542,-0.6,19.7283489784518));
#20873=CARTESIAN_POINT('',(10.5400737530542,-0.5,19.7283489784518));
#20874=CARTESIAN_POINT('Origin',(10.7050737530542,-0.5,19.7283489784518));
#20875=CARTESIAN_POINT('',(10.5400737530542,0.5,19.7283489784518));
#20876=CARTESIAN_POINT('',(10.5400737530542,-0.6,19.7283489784518));
#20877=CARTESIAN_POINT('Origin',(10.7050737530542,0.5,19.7283489784518));
#20878=CARTESIAN_POINT('Origin',(10.7050737530542,-0.6,17.1120538880616));
#20879=CARTESIAN_POINT('',(10.5400737530542,-0.5,17.1120538880616));
#20880=CARTESIAN_POINT('Origin',(10.7050737530542,-0.5,17.1120538880616));
#20881=CARTESIAN_POINT('',(10.5400737530542,0.5,17.1120538880616));
#20882=CARTESIAN_POINT('',(10.5400737530542,-0.6,17.1120538880616));
#20883=CARTESIAN_POINT('Origin',(10.7050737530542,0.5,17.1120538880616));
#20884=CARTESIAN_POINT('Origin',(9.39692620785909,-0.6,18.4202014332567));
#20885=CARTESIAN_POINT('',(7.79692620785909,-0.5,18.4202014332567));
#20886=CARTESIAN_POINT('Origin',(9.39692620785909,-0.5,18.4202014332567));
#20887=CARTESIAN_POINT('',(7.79692620785909,0.5,18.4202014332567));
#20888=CARTESIAN_POINT('',(7.79692620785909,-0.6,18.4202014332567));
#20889=CARTESIAN_POINT('Origin',(9.39692620785909,0.5,18.4202014332567));
#20890=CARTESIAN_POINT('Origin',(9.39692620785909,-0.5,18.4202014332567));
#20891=CARTESIAN_POINT('',(7.81832456572892,0.5,16.8878774285292));
#20892=CARTESIAN_POINT('',(7.81832456572892,-0.5,16.8878774285292));
#20893=CARTESIAN_POINT('',(7.81832456572892,-0.5,16.8878774285292));
#20894=CARTESIAN_POINT('',(7.20268830774272,0.5,18.5793241459439));
#20895=CARTESIAN_POINT('Origin',(9.39692620785909,0.5,18.4202014332567));
#20896=CARTESIAN_POINT('',(7.20268830774272,-0.5,18.5793241459439));
#20897=CARTESIAN_POINT('',(7.20268830774272,-0.5,18.5793241459439));
#20898=CARTESIAN_POINT('Origin',(9.39692620785909,-0.5,18.4202014332567));
#20899=CARTESIAN_POINT('Origin',(4.69846310392954,-0.5,16.7101007166283));
#20900=CARTESIAN_POINT('',(1.57860164213016,-0.5,16.5323240047274));
#20901=CARTESIAN_POINT('',(-0.307818128993102,-0.5,15.8457233587073));
#20902=CARTESIAN_POINT('',(2.19423790011636,-0.5,14.8408772873128));
#20903=CARTESIAN_POINT('Origin',(0.,-0.5,15.));
#20904=CARTESIAN_POINT('',(9.70474433685219,-0.5,17.5744780745494));
#20905=CARTESIAN_POINT('',(-1.6,-0.5,15.));
#20906=CARTESIAN_POINT('Origin',(0.,-0.5,15.));
#20907=CARTESIAN_POINT('',(1.14314754519511,-0.5,13.6918524548049));
#20908=CARTESIAN_POINT('Origin',(1.30814754519511,-0.5,13.6918524548049));
#20909=CARTESIAN_POINT('',(1.14314754519511,-0.5,16.3081475451951));
#20910=CARTESIAN_POINT('Origin',(1.30814754519511,-0.5,16.3081475451951));
#20911=CARTESIAN_POINT('',(-1.47314754519511,-0.5,16.3081475451951));
#20912=CARTESIAN_POINT('Origin',(-1.30814754519511,-0.5,16.3081475451951));
#20913=CARTESIAN_POINT('',(-1.47314754519511,-0.5,13.6918524548049));
#20914=CARTESIAN_POINT('Origin',(-1.30814754519511,-0.5,13.6918524548049));
#20915=CARTESIAN_POINT('Origin',(-0.307818128993102,-0.5,15.8457233587073));
#20916=CARTESIAN_POINT('',(1.57860164213016,0.5,16.5323240047274));
#20917=CARTESIAN_POINT('',(-0.307818128993102,0.5,15.8457233587073));
#20918=CARTESIAN_POINT('',(1.57860164213016,-0.5,16.5323240047274));
#20919=CARTESIAN_POINT('Origin',(-1.30814754519511,-0.6,13.6918524548049));
#20920=CARTESIAN_POINT('',(-1.47314754519511,0.5,13.6918524548049));
#20921=CARTESIAN_POINT('',(-1.47314754519511,-0.6,13.6918524548049));
#20922=CARTESIAN_POINT('Origin',(-1.30814754519511,0.5,13.6918524548049));
#20923=CARTESIAN_POINT('Origin',(-1.30814754519511,-0.6,16.3081475451951));
#20924=CARTESIAN_POINT('',(-1.47314754519511,0.5,16.3081475451951));
#20925=CARTESIAN_POINT('',(-1.47314754519511,-0.6,16.3081475451951));
#20926=CARTESIAN_POINT('Origin',(-1.30814754519511,0.5,16.3081475451951));
#20927=CARTESIAN_POINT('Origin',(1.30814754519511,-0.6,16.3081475451951));
#20928=CARTESIAN_POINT('',(1.14314754519511,0.5,16.3081475451951));
#20929=CARTESIAN_POINT('',(1.14314754519511,-0.6,16.3081475451951));
#20930=CARTESIAN_POINT('Origin',(1.30814754519511,0.5,16.3081475451951));
#20931=CARTESIAN_POINT('Origin',(1.30814754519511,-0.6,13.6918524548049));
#20932=CARTESIAN_POINT('',(1.14314754519511,0.5,13.6918524548049));
#20933=CARTESIAN_POINT('',(1.14314754519511,-0.6,13.6918524548049));
#20934=CARTESIAN_POINT('Origin',(1.30814754519511,0.5,13.6918524548049));
#20935=CARTESIAN_POINT('Origin',(0.,-0.6,15.));
#20936=CARTESIAN_POINT('',(-1.6,0.5,15.));
#20937=CARTESIAN_POINT('',(-1.6,-0.6,15.));
#20938=CARTESIAN_POINT('Origin',(0.,0.5,15.));
#20939=CARTESIAN_POINT('Origin',(0.,-0.5,15.));
#20940=CARTESIAN_POINT('',(2.19423790011636,0.5,14.8408772873128));
#20941=CARTESIAN_POINT('',(2.19423790011636,-0.5,14.8408772873128));
#20942=CARTESIAN_POINT('Origin',(0.,0.5,15.));
#20943=CARTESIAN_POINT('Origin',(9.70474433685219,-0.5,17.5744780745494));
#20944=CARTESIAN_POINT('',(9.70474433685219,0.5,17.5744780745494));
#20945=CARTESIAN_POINT('Origin',(4.69846310392954,0.5,16.7101007166283));
#23528=UNCERTAINTY_MEASURE_WITH_UNIT(LENGTH_MEASURE(0.001),#23729,
'DISTANCE_ACCURACY_VALUE',
'Maximum model space distance between geometric entities at asserted c
onnectivities');
#23611=UNCERTAINTY_MEASURE_WITH_UNIT(LENGTH_MEASURE(0.001),#23729,
'DISTANCE_ACCURACY_VALUE',
'Maximum model space distance between geometric entities at asserted c
onnectivities');
#23645=(
GEOMETRIC_REPRESENTATION_CONTEXT(3)
GLOBAL_UNCERTAINTY_ASSIGNED_CONTEXT((#23528))
GLOBAL_UNIT_ASSIGNED_CONTEXT((#23729,#23731,#23732))
REPRESENTATION_CONTEXT('','3D')
);
#23728=(
GEOMETRIC_REPRESENTATION_CONTEXT(3)
GLOBAL_UNCERTAINTY_ASSIGNED_CONTEXT((#23611))
GLOBAL_UNIT_ASSIGNED_CONTEXT((#23729,#23731,#23732))
REPRESENTATION_CONTEXT('','3D')
);
#23729=(
LENGTH_UNIT()
NAMED_UNIT(*)
SI_UNIT(.CENTI.,.METRE.)
);
#23731=(
NAMED_UNIT(*)
PLANE_ANGLE_UNIT()
SI_UNIT($,.RADIAN.)
);
#23732=(
NAMED_UNIT(*)
SI_UNIT($,.STERADIAN.)
SOLID_ANGLE_UNIT()
);
#23766=SHAPE_DEFINITION_REPRESENTATION(#23882,#24145);
#23882=PRODUCT_DEFINITION_SHAPE('',$,#24262);
#24145=SHAPE_REPRESENTATION('',(#14202),#23645);
#24228=PRODUCT_DEFINITION_CONTEXT('part definition',#24578,'design');
#24262=PRODUCT_DEFINITION('Input link (1)','Input link (1)',#24378,#24228);
#24378=PRODUCT_DEFINITION_FORMATION('',$,#24613);
#24578=APPLICATION_CONTEXT(
'Core Data for Automotive Mechanical Design Process');
#24579=PRODUCT_CONTEXT('part definition',#24578,'mechanical');
#24613=PRODUCT('Input link (1)','Input link (1)','Input link (1)',(#24579));
#24773=COLOUR_RGB('Off White',0.89,0.88,0.83);
#24774=FILL_AREA_STYLE_COLOUR('',#24773);
#24775=FILL_AREA_STYLE('',(#24774));
#24776=SURFACE_STYLE_FILL_AREA(#24775);
#24777=SURFACE_SIDE_STYLE('',(#24776));
#24778=SURFACE_STYLE_USAGE(.BOTH.,#24777);
#24779=PRESENTATION_STYLE_ASSIGNMENT((#24778));
ENDSEC;
END-ISO-10303-21;
